ISO-10303-21;
HEADER;
FILE_DESCRIPTION (('STEP AP203'),
    '1' );
FILE_NAME ('Fixed base.step',
    '2026-10-31T14:11:27',
    ( '' ),
    ( '' ),
    'SwSTEP 2.0',
    'SolidWorks 2024',
    '' );
FILE_SCHEMA (( 'AUTOMOTIVE_DESIGN' ));
ENDSEC;

DATA;
#69=FACE_OUTER_BOUND ( 'NONE', #8738, .T. ) ;
#115=VERTEX_POINT ( 'NONE', #8937 ) ;
#165=CARTESIAN_POINT ( 'NONE',  ( 43.84419854219520829, -31.09999999999999787, 21.49999999999999289 ) ) ;
#200=DIRECTION ( 'NONE',  ( -6.123237832262829536E-17, -1.734723475976808278E-15, 1.000000000000000000 ) ) ;
#250=VECTOR ( 'NONE', #1916, 1000.000000000000000 ) ;
#258=VECTOR ( 'NONE', #13231, 1000.000000000000000 ) ;
#290=VERTEX_POINT ( 'NONE', #14509 ) ;
#295=VECTOR ( 'NONE', #19541, 1000.000000000000000 ) ;
#378=CIRCLE ( 'NONE', #15561, 4.099999999999999645 ) ;
#403=CARTESIAN_POINT ( 'NONE',  ( -25.00842861987479893, -15.87143667223269894, 25.00000000000000000 ) ) ;
#415=DIRECTION ( 'NONE',  ( 1.000000000000000000, 0.000000000000000000, 0.000000000000000000 ) ) ;
#421=DIRECTION ( 'NONE',  ( -1.000000000000000000, 0.000000000000000000, 0.000000000000000000 ) ) ;
#491=FACE_OUTER_BOUND ( 'NONE', #938, .T. ) ;
#519=VECTOR ( 'NONE', #21542, 1000.000000000000000 ) ;
#533=DIRECTION ( 'NONE',  ( -1.000000000000000000, 0.000000000000000000, 0.000000000000000000 ) ) ;
#548=DIRECTION ( 'NONE',  ( -0.000000000000000000, -0.000000000000000000, 1.000000000000000000 ) ) ;
#579=ORIENTED_EDGE ( 'NONE', *, *, #4356, .F. ) ;
#650=CARTESIAN_POINT ( 'NONE',  ( 43.84419854219520829, -31.09999999999999787, -21.50000000000000000 ) ) ;
#690=LINE ( 'NONE', #3920, #15989 ) ;
#719=VERTEX_POINT ( 'NONE', #5890 ) ;
#841=CARTESIAN_POINT ( 'NONE',  ( -26.99999999999959854, -31.09999999999999787, -22.00000000000000000 ) ) ;
#919=EDGE_CURVE ( 'NONE', #8630, #18569, #15543, .T. ) ;
#938=EDGE_LOOP ( 'NONE', ( #15699, #5790, #23257, #12732, #11651 ) ) ;
#1017=VERTEX_POINT ( 'NONE', #18105 ) ;
#1149=DIRECTION ( 'NONE',  ( -1.000000000000000000, 0.000000000000000000, 0.000000000000000000 ) ) ;
#1185=DIRECTION ( 'NONE',  ( 2.977235988022388482E-185, -9.605990953944227443E-124, -1.000000000000000000 ) ) ;
#1218=EDGE_CURVE ( 'NONE', #8630, #115, #21883, .T. ) ;
#1275=EDGE_CURVE ( 'NONE', #719, #23466, #12871, .T. ) ;
#1341=( GEOMETRIC_REPRESENTATION_CONTEXT ( 3 ) GLOBAL_UNCERTAINTY_ASSIGNED_CONTEXT ( ( #13396 ) ) GLOBAL_UNIT_ASSIGNED_CONTEXT ( ( #9824, #11156, #18383 ) ) REPRESENTATION_CONTEXT ( 'NONE', 'WORKASPACE' ) );
#1361=DIRECTION ( 'NONE',  ( 0.9999997101582432935, 0.0007613694435018768464, -1.641484103780244428E-33 ) ) ;
#1403=DIRECTION ( 'NONE',  ( -1.000000000000000000, 0.000000000000000000, 0.000000000000000000 ) ) ;
#1416=CARTESIAN_POINT ( 'NONE',  ( -22.99999999999959854, -19.33065833018789803, 23.00000000000000000 ) ) ;
#1418=LINE ( 'NONE', #12600, #14530 ) ;
#1424=EDGE_LOOP ( 'NONE', ( #7638, #12374, #2876, #22818, #17334 ) ) ;
#1431=ORIENTED_EDGE ( 'NONE', *, *, #11942, .T. ) ;
#1565=LINE ( 'NONE', #10749, #4566 ) ;
#1616=AXIS2_PLACEMENT_3D ( 'NONE', #21479, #200, #1872 ) ;
#1623=AXIS2_PLACEMENT_3D ( 'NONE', #20579, #11589, #18816 ) ;
#1624=VECTOR ( 'NONE', #2774, 1000.000000000000000 ) ;
#1659=FACE_OUTER_BOUND ( 'NONE', #16445, .T. ) ;
#1698=EDGE_LOOP ( 'NONE', ( #2794, #17614, #14991, #6792 ) ) ;
#1740=CARTESIAN_POINT ( 'NONE',  ( -26.99999999999959854, -31.09999999999999787, -21.50000000000000000 ) ) ;
#1764=EDGE_CURVE ( 'NONE', #290, #6621, #7398, .T. ) ;
#1789=CARTESIAN_POINT ( 'NONE',  ( 3.242007008979478005E-15, -33.09999999999999432, 25.00000000000000000 ) ) ;
#1872=DIRECTION ( 'NONE',  ( 0.000000000000000000, -1.000000000000000000, -1.734723475976808278E-15 ) ) ;
#1875=CIRCLE ( 'NONE', #15147, 4.000000000000000000 ) ;
#1897=AXIS2_PLACEMENT_3D ( 'NONE', #18802, #21976, #20446 ) ;
#1916=DIRECTION ( 'NONE',  ( 6.123237831918399306E-17, -1.569224110909209817E-30, -1.000000000000000000 ) ) ;
#1989=ORIENTED_EDGE ( 'NONE', *, *, #12764, .T. ) ;
#2007=FACE_OUTER_BOUND ( 'NONE', #20434, .T. ) ;
#2011=ADVANCED_FACE ( 'NONE', ( #19360 ), #10357, .T. ) ;
#2024=AXIS2_PLACEMENT_3D ( 'NONE', #6807, #15715, #6696 ) ;
#2079=DIRECTION ( 'NONE',  ( -2.977235988022388482E-185, 9.605990953944227443E-124, 1.000000000000000000 ) ) ;
#2084=DIRECTION ( 'NONE',  ( 0.000000000000000000, 0.000000000000000000, 1.000000000000000000 ) ) ;
#2096=CARTESIAN_POINT ( 'NONE',  ( 43.84419854219520118, 9.774809681453278998, 25.00000000000000000 ) ) ;
#2106=EDGE_LOOP ( 'NONE', ( #2283, #19043, #9151, #21840 ) ) ;
#2111=ORIENTED_EDGE ( 'NONE', *, *, #20825, .T. ) ;
#2147=AXIS2_PLACEMENT_3D ( 'NONE', #7748, #16634, #4176 ) ;
#2156=FACE_OUTER_BOUND ( 'NONE', #8635, .T. ) ;
#2198=ORIENTED_EDGE ( 'NONE', *, *, #9767, .T. ) ;
#2204=ADVANCED_FACE ( 'NONE', ( #2007 ), #14481, .F. ) ;
#2231=CARTESIAN_POINT ( 'NONE',  ( 35.59419854219520118, 9.774809681453278998, -25.00000000000000000 ) ) ;
#2275=CARTESIAN_POINT ( 'NONE',  ( -26.99999999999959854, -19.33065833018799751, -21.50000000000000000 ) ) ;
#2283=ORIENTED_EDGE ( 'NONE', *, *, #21029, .T. ) ;
#2306=DIRECTION ( 'NONE',  ( -1.320147222947483248E-46, 2.155962677239134989E-30, 1.000000000000000000 ) ) ;
#2426=CARTESIAN_POINT ( 'NONE',  ( 31.45181451370270054, 16.90945435098589655, 23.00000000000000000 ) ) ;
#2521=ORIENTED_EDGE ( 'NONE', *, *, #13591, .T. ) ;
#2551=DIRECTION ( 'NONE',  ( -6.123237831918399306E-17, 1.569224110909209817E-30, 1.000000000000000000 ) ) ;
#2569=CARTESIAN_POINT ( 'NONE',  ( 0.000000000000000000, 0.000000000000000000, 0.000000000000000000 ) ) ;
#2581=ORIENTED_EDGE ( 'NONE', *, *, #9104, .F. ) ;
#2590=DIRECTION ( 'NONE',  ( 6.123237831918399306E-17, -1.590047762086094914E-30, -1.000000000000000000 ) ) ;
#2627=CARTESIAN_POINT ( 'NONE',  ( 35.59419854219520118, 9.774809681453278998, -23.00000000000000000 ) ) ;
#2647=LINE ( 'NONE', #2426, #1624 ) ;
#2666=VERTEX_POINT ( 'NONE', #17277 ) ;
#2691=DIRECTION ( 'NONE',  ( 2.977235988022388482E-185, -9.605990953944227443E-124, -1.000000000000000000 ) ) ;
#2698=ORIENTED_EDGE ( 'NONE', *, *, #18662, .T. ) ;
#2732=ORIENTED_EDGE ( 'NONE', *, *, #18565, .T. ) ;
#2749=CYLINDRICAL_SURFACE ( 'NONE', #23026, 4.099999999999999645 ) ;
#2752=ORIENTED_EDGE ( 'NONE', *, *, #1218, .T. ) ;
#2774=DIRECTION ( 'NONE',  ( -6.123237831918399306E-17, 1.569224110909209817E-30, 1.000000000000000000 ) ) ;
#2794=ORIENTED_EDGE ( 'NONE', *, *, #5329, .T. ) ;
#2814=CARTESIAN_POINT ( 'NONE',  ( 31.45181451370269343, 16.90945435098590011, -21.50000000000000000 ) ) ;
#2876=ORIENTED_EDGE ( 'NONE', *, *, #5000, .T. ) ;
#2880=EDGE_LOOP ( 'NONE', ( #18097, #579 ) ) ;
#2882=PLANE ( 'NONE',  #9235 ) ;
#2937=CARTESIAN_POINT ( 'NONE',  ( -22.99999999999959854, -19.33065833018789803, -23.00000000000000000 ) ) ;
#3037=PLANE ( 'NONE',  #18126 ) ;
#3104=DIRECTION ( 'NONE',  ( 6.123237831918399306E-17, -1.569224110909209817E-30, -1.000000000000000000 ) ) ;
#3246=LINE ( 'NONE', #19405, #9580 ) ;
#3315=FACE_OUTER_BOUND ( 'NONE', #10843, .T. ) ;
#3491=ORIENTED_EDGE ( 'NONE', *, *, #1275, .T. ) ;
#3518=VECTOR ( 'NONE', #2084, 1000.000000000000000 ) ;
#3612=ORIENTED_EDGE ( 'NONE', *, *, #4711, .T. ) ;
#3632=VERTEX_POINT ( 'NONE', #8745 ) ;
#3757=CARTESIAN_POINT ( 'NONE',  ( 31.45181451370270054, 16.90945435098589655, -23.00000000000000000 ) ) ;
#3920=CARTESIAN_POINT ( 'NONE',  ( 43.81897180516431689, 0.03336243584794939404, -21.50000000000000000 ) ) ;
#3957=ORIENTED_EDGE ( 'NONE', *, *, #18643, .T. ) ;
#4044=DIRECTION ( 'NONE',  ( -1.000000000000000000, 0.000000000000000000, 0.000000000000000000 ) ) ;
#4050=EDGE_CURVE ( 'NONE', #23466, #290, #4344, .T. ) ;
#4060=DIRECTION ( 'NONE',  ( -8.326672684687908612E-17, -1.000000000000000000, 1.564125491189519930E-30 ) ) ;
#4069=EDGE_CURVE ( 'NONE', #115, #12698, #18726, .T. ) ;
#4072=PLANE ( 'NONE',  #1623 ) ;
#4078=CARTESIAN_POINT ( 'NONE',  ( 31.45181451370270054, 16.90945435098589655, -23.00000000000000000 ) ) ;
#4157=AXIS2_PLACEMENT_3D ( 'NONE', #15111, #9788, #14880 ) ;
#4176=DIRECTION ( 'NONE',  ( 1.000000000000000000, 3.099353312215988811E-62, 0.000000000000000000 ) ) ;
#4292=DIRECTION ( 'NONE',  ( 6.123237831918399306E-17, -1.569224110909209817E-30, -1.000000000000000000 ) ) ;
#4323=CARTESIAN_POINT ( 'NONE',  ( 31.49419854219519976, 9.774809681453278998, -25.00000000000000000 ) ) ;
#4344=LINE ( 'NONE', #22140, #20966 ) ;
#4356=EDGE_CURVE ( 'NONE', #20891, #8556, #11123, .T. ) ;
#4397=LINE ( 'NONE', #9867, #18192 ) ;
#4468=CARTESIAN_POINT ( 'NONE',  ( 43.81897180516431689, 0.03336243584794939404, -25.00000000000000000 ) ) ;
#4540=LINE ( 'NONE', #18925, #15299 ) ;
#4562=VERTEX_POINT ( 'NONE', #15226 ) ;
#4566=VECTOR ( 'NONE', #17983, 1000.000000000000000 ) ;
#4706=CARTESIAN_POINT ( 'NONE',  ( -26.99999999999961631, -1.360632482642508324E-14, -21.50000000000000000 ) ) ;
#4711=EDGE_CURVE ( 'NONE', #19959, #12698, #11803, .T. ) ;
#4884=ORIENTED_EDGE ( 'NONE', *, *, #8732, .F. ) ;
#4922=CARTESIAN_POINT ( 'NONE',  ( 43.84419854219520829, -33.09999999999998721, -25.00000000000000000 ) ) ;
#4923=ORIENTED_EDGE ( 'NONE', *, *, #18232, .F. ) ;
#4970=EDGE_CURVE ( 'NONE', #11110, #19959, #1875, .T. ) ;
#5000=EDGE_CURVE ( 'NONE', #18569, #8287, #4397, .T. ) ;
#5112=DIRECTION ( 'NONE',  ( -6.123237831918399306E-17, 1.590047762086094914E-30, 1.000000000000000000 ) ) ;
#5233=LINE ( 'NONE', #8923, #21512 ) ;
#5243=CARTESIAN_POINT ( 'NONE',  ( -4.620515280316187769E-46, 7.545869370336972286E-30, -21.50000000000000000 ) ) ;
#5310=AXIS2_PLACEMENT_3D ( 'NONE', #10130, #1185, #15805 ) ;
#5329=EDGE_CURVE ( 'NONE', #11214, #2666, #8668, .T. ) ;
#5348=SHAPE_REPRESENTATION ( 'Fixed base', ( #12739 ), #1341 ) ;
#5385=ORIENTED_EDGE ( 'NONE', *, *, #6086, .F. ) ;
#5399=AXIS2_PLACEMENT_3D ( 'NONE', #23422, #14288, #5725 ) ;
#5437=ORIENTED_EDGE ( 'NONE', *, *, #15135, .F. ) ;
#5453=PLANE ( 'NONE',  #1616 ) ;
#5469=EDGE_CURVE ( 'NONE', #16018, #15497, #378, .T. ) ;
#5511=AXIS2_PLACEMENT_3D ( 'NONE', #2231, #22180, #15301 ) ;
#5529=CARTESIAN_POINT ( 'NONE',  ( 43.81210844073630994, 9.047859270861110303, -21.50000000000000000 ) ) ;
#5566=CIRCLE ( 'NONE', #19223, 4.000000000000000000 ) ;
#5578=ORIENTED_EDGE ( 'NONE', *, *, #5329, .F. ) ;
#5644=CARTESIAN_POINT ( 'NONE',  ( 43.84419854219520829, -33.09999999999998721, -65.86501949894326913 ) ) ;
#5676=DIRECTION ( 'NONE',  ( -6.123237831918399306E-17, 1.569224110909209817E-30, 1.000000000000000000 ) ) ;
#5693=CIRCLE ( 'NONE', #5310, 8.250000000000000000 ) ;
#5725=DIRECTION ( 'NONE',  ( -1.000000000000000000, 0.000000000000000000, 0.000000000000000000 ) ) ;
#5763=CARTESIAN_POINT ( 'NONE',  ( 35.59419854219520118, 9.774809681453278998, 25.00000000000000000 ) ) ;
#5790=ORIENTED_EDGE ( 'NONE', *, *, #20292, .T. ) ;
#5808=VERTEX_POINT ( 'NONE', #4922 ) ;
#5831=DIRECTION ( 'NONE',  ( 0.0007613694435018767380, -0.9999997101582432935, 0.000000000000000000 ) ) ;
#5842=AXIS2_PLACEMENT_3D ( 'NONE', #18385, #11028, #12796 ) ;
#5880=CARTESIAN_POINT ( 'NONE',  ( 31.45181451370270054, 16.90945435098589655, -25.00000000000000000 ) ) ;
#5890=CARTESIAN_POINT ( 'NONE',  ( -26.99999999999959854, -19.33065833018799751, -25.00000000000000000 ) ) ;
#5936=ORIENTED_EDGE ( 'NONE', *, *, #4970, .T. ) ;
#5952=ORIENTED_EDGE ( 'NONE', *, *, #12764, .F. ) ;
#5964=EDGE_LOOP ( 'NONE', ( #22787, #22650, #18178, #5952, #12618, #15544 ) ) ;
#6013=AXIS2_PLACEMENT_3D ( 'NONE', #7804, #548, #421 ) ;
#6027=ORIENTED_EDGE ( 'NONE', *, *, #919, .T. ) ;
#6032=VERTEX_POINT ( 'NONE', #8124 ) ;
#6073=PLANE ( 'NONE',  #2147 ) ;
#6086=EDGE_CURVE ( 'NONE', #17891, #19315, #22350, .T. ) ;
#6157=AXIS2_PLACEMENT_3D ( 'NONE', #11013, #18243, #14323 ) ;
#6209=EDGE_LOOP ( 'NONE', ( #4923, #8151, #14860, #5385 ) ) ;
#6247=EDGE_LOOP ( 'NONE', ( #17779, #16109, #21613, #23021 ) ) ;
#6260=VECTOR ( 'NONE', #5676, 1000.000000000000000 ) ;
#6311=FACE_OUTER_BOUND ( 'NONE', #1698, .T. ) ;
#6336=VECTOR ( 'NONE', #20450, 1000.000000000000000 ) ;
#6377=LINE ( 'NONE', #16942, #14659 ) ;
#6386=CYLINDRICAL_SURFACE ( 'NONE', #10356, 3.999999999999998668 ) ;
#6405=CIRCLE ( 'NONE', #11688, 8.250000000000003553 ) ;
#6509=DIRECTION ( 'NONE',  ( 0.000000000000000000, 0.000000000000000000, 1.000000000000000000 ) ) ;
#6514=ADVANCED_FACE ( 'NONE', ( #7970 ), #18792, .F. ) ;
#6595=DIRECTION ( 'NONE',  ( 6.123237831918399306E-17, -1.569224110909209817E-30, -1.000000000000000000 ) ) ;
#6621=VERTEX_POINT ( 'NONE', #9399 ) ;
#6696=DIRECTION ( 'NONE',  ( 0.5021071549687922131, -0.8648054144888001060, 0.000000000000000000 ) ) ;
#6756=CARTESIAN_POINT ( 'NONE',  ( 43.84419854219520829, 0.000000000000000000, -65.86501949894326913 ) ) ;
#6792=ORIENTED_EDGE ( 'NONE', *, *, #14829, .T. ) ;
#6807=CARTESIAN_POINT ( 'NONE',  ( -22.99999999999959854, -19.33065833018789803, 25.00000000000000000 ) ) ;
#6835=ORIENTED_EDGE ( 'NONE', *, *, #21686, .T. ) ;
#6848=FACE_OUTER_BOUND ( 'NONE', #1424, .T. ) ;
#6870=FACE_OUTER_BOUND ( 'NONE', #23428, .T. ) ;
#6955=ADVANCED_FACE ( 'NONE', ( #3315 ), #5453, .F. ) ;
#6984=AXIS2_PLACEMENT_3D ( 'NONE', #17889, #8749, #15871 ) ;
#7086=CARTESIAN_POINT ( 'NONE',  ( 39.69419854219519550, 9.774809681453278998, 23.00000000000000000 ) ) ;
#7093=EDGE_CURVE ( 'NONE', #17221, #1017, #19452, .T. ) ;
#7096=DIRECTION ( 'NONE',  ( 0.000000000000000000, 1.000000000000000000, -9.605990953944227443E-124 ) ) ;
#7112=LINE ( 'NONE', #1740, #13232 ) ;
#7134=DIRECTION ( 'NONE',  ( 0.5021071549687922131, -0.8648054144888001060, 0.000000000000000000 ) ) ;
#7137=DIRECTION ( 'NONE',  ( 0.000000000000000000, 0.000000000000000000, 1.000000000000000000 ) ) ;
#7143=DIRECTION ( 'NONE',  ( 1.000000000000000000, 6.123237831918419028E-17, 0.000000000000000000 ) ) ;
#7219=DIRECTION ( 'NONE',  ( 0.8648054144888007722, 0.5021071549687909918, -4.823236788540877710E-124 ) ) ;
#7227=DIRECTION ( 'NONE',  ( -0.5021071549687922131, 0.8648054144888001060, 0.000000000000000000 ) ) ;
#7280=DIRECTION ( 'NONE',  ( 0.8648054144888008832, 0.5021071549687909918, 0.000000000000000000 ) ) ;
#7285=LINE ( 'NONE', #21517, #250 ) ;
#7398=LINE ( 'NONE', #1789, #16312 ) ;
#7434=ORIENTED_EDGE ( 'NONE', *, *, #8913, .F. ) ;
#7461=AXIS2_PLACEMENT_3D ( 'NONE', #11566, #7974, #7227 ) ;
#7475=LINE ( 'NONE', #14708, #6260 ) ;
#7496=VECTOR ( 'NONE', #15751, 1000.000000000000000 ) ;
#7576=DIRECTION ( 'NONE',  ( 6.123237831918399306E-17, -1.569224110909209817E-30, -1.000000000000000000 ) ) ;
#7638=ORIENTED_EDGE ( 'NONE', *, *, #11942, .F. ) ;
#7741=EDGE_CURVE ( 'NONE', #17836, #13324, #1418, .T. ) ;
#7748=CARTESIAN_POINT ( 'NONE',  ( -27.00000000000000000, -31.09999999999999787, 21.50000000000000000 ) ) ;
#7804=CARTESIAN_POINT ( 'NONE',  ( 35.59419854219520118, 9.774809681453278998, -21.50000000000000000 ) ) ;
#7818=ORIENTED_EDGE ( 'NONE', *, *, #4069, .F. ) ;
#7936=ORIENTED_EDGE ( 'NONE', *, *, #22988, .F. ) ;
#7966=ORIENTED_EDGE ( 'NONE', *, *, #22295, .T. ) ;
#7970=FACE_OUTER_BOUND ( 'NONE', #6247, .T. ) ;
#7974=DIRECTION ( 'NONE',  ( -6.123237831918399306E-17, 1.586917373610080078E-30, 1.000000000000000000 ) ) ;
#7985=DIRECTION ( 'NONE',  ( -1.000000000000000000, 8.326672684687908612E-17, 0.000000000000000000 ) ) ;
#8019=DIRECTION ( 'NONE',  ( -0.8648054144888007722, -0.5021071549687909918, -5.295409231245618283E-17 ) ) ;
#8029=CARTESIAN_POINT ( 'NONE',  ( 35.59419854219520118, 9.774809681453278998, -21.50000000000000000 ) ) ;
#8077=ORIENTED_EDGE ( 'NONE', *, *, #18565, .F. ) ;
#8124=CARTESIAN_POINT ( 'NONE',  ( 43.84419854219520829, -33.09999999999999432, -21.50000000000000000 ) ) ;
#8151=ORIENTED_EDGE ( 'NONE', *, *, #4356, .T. ) ;
#8194=ORIENTED_EDGE ( 'NONE', *, *, #7093, .F. ) ;
#8287=VERTEX_POINT ( 'NONE', #16120 ) ;
#8291=FACE_OUTER_BOUND ( 'NONE', #21994, .T. ) ;
#8460=AXIS2_PLACEMENT_3D ( 'NONE', #17405, #12077, #10174 ) ;
#8485=ADVANCED_FACE ( 'NONE', ( #69 ), #11164, .T. ) ;
#8506=ORIENTED_EDGE ( 'NONE', *, *, #9767, .F. ) ;
#8507=FACE_OUTER_BOUND ( 'NONE', #13148, .T. ) ;
#8556=VERTEX_POINT ( 'NONE', #10920 ) ;
#8627=DIRECTION ( 'NONE',  ( -1.000000000000000000, -3.593595090780715053E-30, -6.123237832262829536E-17 ) ) ;
#8630=VERTEX_POINT ( 'NONE', #2814 ) ;
#8635=EDGE_LOOP ( 'NONE', ( #8077, #17509, #8983, #13895, #13787, #2198 ) ) ;
#8668=LINE ( 'NONE', #403, #21571 ) ;
#8732=EDGE_CURVE ( 'NONE', #13324, #6621, #13261, .T. ) ;
#8738=EDGE_LOOP ( 'NONE', ( #23306, #19698, #8506, #15844 ) ) ;
#8745=CARTESIAN_POINT ( 'NONE',  ( -26.99999999999959854, -31.09999999999999787, -21.50000000000000000 ) ) ;
#8749=DIRECTION ( 'NONE',  ( -1.000000000000000000, -4.040376328279780192E-15, -6.123237831918399306E-17 ) ) ;
#8913=EDGE_CURVE ( 'NONE', #1017, #15497, #19899, .T. ) ;
#8923=CARTESIAN_POINT ( 'NONE',  ( 43.84419854219520829, -33.09999999999998721, -21.50000000000000000 ) ) ;
#8937=CARTESIAN_POINT ( 'NONE',  ( 31.45181451370270054, 16.90945435098589655, -25.00000000000000000 ) ) ;
#8961=ORIENTED_EDGE ( 'NONE', *, *, #12135, .T. ) ;
#8983=ORIENTED_EDGE ( 'NONE', *, *, #16245, .T. ) ;
#9001=LINE ( 'NONE', #16234, #21442 ) ;
#9005=DIRECTION ( 'NONE',  ( -1.000000000000000000, -1.296622928517386003E-46, 0.000000000000000000 ) ) ;
#9011=ORIENTED_EDGE ( 'NONE', *, *, #18938, .T. ) ;
#9025=CARTESIAN_POINT ( 'NONE',  ( 35.59419854219520118, 9.774809681453278998, 23.00000000000000000 ) ) ;
#9071=ORIENTED_EDGE ( 'NONE', *, *, #21461, .F. ) ;
#9104=EDGE_CURVE ( 'NONE', #23466, #5808, #20599, .T. ) ;
#9147=ORIENTED_EDGE ( 'NONE', *, *, #4711, .F. ) ;
#9151=ORIENTED_EDGE ( 'NONE', *, *, #21731, .F. ) ;
#9197=ADVANCED_FACE ( 'NONE', ( #17149, #20358 ), #20253, .F. ) ;
#9235=AXIS2_PLACEMENT_3D ( 'NONE', #5243, #14384, #13058 ) ;
#9262=DIRECTION ( 'NONE',  ( -1.000000000000000000, 0.000000000000000000, 0.000000000000000000 ) ) ;
#9270=ORIENTED_EDGE ( 'NONE', *, *, #12055, .F. ) ;
#9377=PRODUCT_DEFINITION ( 'UNKNOWN', '', #17948, #18010 ) ;
#9398=VERTEX_POINT ( 'NONE', #21759 ) ;
#9399=CARTESIAN_POINT ( 'NONE',  ( 43.84419854219520829, -33.09999999999998721, 25.00000000000000000 ) ) ;
#9462=CARTESIAN_POINT ( 'NONE',  ( -26.99999999999959854, -33.09999999999999432, -25.00000000000000000 ) ) ;
#9483=ORIENTED_EDGE ( 'NONE', *, *, #11180, .F. ) ;
#9535=CARTESIAN_POINT ( 'NONE',  ( 5.000000000000180300, -33.09999999999999432, -22.00000000000000000 ) ) ;
#9544=EDGE_CURVE ( 'NONE', #17474, #9398, #1565, .T. ) ;
#9580=VECTOR ( 'NONE', #6595, 1000.000000000000000 ) ;
#9601=CIRCLE ( 'NONE', #18307, 4.100000000000000533 ) ;
#9673=ADVANCED_FACE ( 'NONE', ( #11219 ), #22456, .F. ) ;
#9738=DIRECTION ( 'NONE',  ( -2.977235988022388482E-185, 9.605990953944227443E-124, 1.000000000000000000 ) ) ;
#9746=ORIENTED_EDGE ( 'NONE', *, *, #14381, .F. ) ;
#9759=CARTESIAN_POINT ( 'NONE',  ( -22.99999999999959854, -19.33065833018789803, -21.50000000000000000 ) ) ;
#9767=EDGE_CURVE ( 'NONE', #21997, #17836, #5693, .T. ) ;
#9788=DIRECTION ( 'NONE',  ( -6.123237831918399306E-17, 2.152213273084510109E-30, 1.000000000000000000 ) ) ;
#9824=( LENGTH_UNIT ( ) NAMED_UNIT ( * ) SI_UNIT ( .MILLI., .METRE. ) );
#9843=CARTESIAN_POINT ( 'NONE',  ( -25.00842861987481314, -15.87143667223275401, -21.50000000000000000 ) ) ;
#9854=ADVANCED_FACE ( 'NONE', ( #6311 ), #21142, .T. ) ;
#9867=CARTESIAN_POINT ( 'NONE',  ( 43.81897180516431689, 0.03336243584794939404, -21.50000000000000000 ) ) ;
#9880=ADVANCED_FACE ( 'NONE', ( #1659, #11272 ), #23145, .T. ) ;
#9913=CLOSED_SHELL ( 'NONE', ( #2204, #6514, #14587, #19654, #19450, #8485, #14576, #13174, #19916, #20531, #13401, #9197, #9673, #18421, #2011, #9854, #9880, #23141, #13616, #6955 ) ) ;
#9971=DIRECTION ( 'NONE',  ( -0.5021071549687922131, 0.8648054144888001060, 0.000000000000000000 ) ) ;
#10036=EDGE_LOOP ( 'NONE', ( #21953, #9147, #1989, #2752 ) ) ;
#10130=CARTESIAN_POINT ( 'NONE',  ( 35.59419854219520118, 9.774809681453278998, 21.49999999999999289 ) ) ;
#10160=VECTOR ( 'NONE', #22803, 1000.000000000000000 ) ;
#10174=DIRECTION ( 'NONE',  ( 0.6660003063074656504, -0.7459514675891198987, 0.000000000000000000 ) ) ;
#10176=ORIENTED_EDGE ( 'NONE', *, *, #1218, .F. ) ;
#10180=MECHANICAL_CONTEXT ( 'NONE', #16698, 'mechanical' ) ;
#10201=LINE ( 'NONE', #23337, #14519 ) ;
#10272=CARTESIAN_POINT ( 'NONE',  ( -25.00842861987479893, -15.87143667223269894, -25.00000000000000000 ) ) ;
#10307=CARTESIAN_POINT ( 'NONE',  ( 86.89068504225697609, -31.09999999999999787, -21.49999999999999645 ) ) ;
#10356=AXIS2_PLACEMENT_3D ( 'NONE', #2937, #2590, #9971 ) ;
#10357=CYLINDRICAL_SURFACE ( 'NONE', #14651, 3.999999999999998668 ) ;
#10550=FACE_OUTER_BOUND ( 'NONE', #22804, .T. ) ;
#10596=ORIENTED_EDGE ( 'NONE', *, *, #7741, .T. ) ;
#10657=VERTEX_POINT ( 'NONE', #11485 ) ;
#10681=DIRECTION ( 'NONE',  ( -6.123237831918669245E-17, 0.000000000000000000, 1.000000000000000000 ) ) ;
#10714=ORIENTED_EDGE ( 'NONE', *, *, #22896, .T. ) ;
#10749=CARTESIAN_POINT ( 'NONE',  ( -26.99999999999959854, -19.33065833018799751, 23.00000000000000000 ) ) ;
#10758=AXIS2_PLACEMENT_3D ( 'NONE', #13171, #9738, #20408 ) ;
#10843=EDGE_LOOP ( 'NONE', ( #5437, #14475, #16667 ) ) ;
#10866=CARTESIAN_POINT ( 'NONE',  ( 0.5868595415223922807, -1.010778882616252483, -21.50000000000000000 ) ) ;
#10901=CARTESIAN_POINT ( 'NONE',  ( 31.49419854219519976, 9.774809681453278998, 21.49999999999999289 ) ) ;
#10905=DIRECTION ( 'NONE',  ( 0.000000000000000000, -1.000000000000000000, 0.000000000000000000 ) ) ;
#10920=CARTESIAN_POINT ( 'NONE',  ( 31.49419854219519976, 9.774809681453278998, -21.50000000000000000 ) ) ;
#10931=CARTESIAN_POINT ( 'NONE',  ( 39.69419854219519550, 9.774809681453278998, -23.00000000000000000 ) ) ;
#10993=CARTESIAN_POINT ( 'NONE',  ( -26.99999999999959854, -19.33065833018799751, -25.00000000000000000 ) ) ;
#11013=CARTESIAN_POINT ( 'NONE',  ( 35.59419854219520118, 9.774809681453278998, -25.00000000000000000 ) ) ;
#11028=DIRECTION ( 'NONE',  ( -6.123237831918409167E-17, 1.616838880122404932E-30, 1.000000000000000000 ) ) ;
#11110=VERTEX_POINT ( 'NONE', #2275 ) ;
#11116=AXIS2_PLACEMENT_3D ( 'NONE', #13134, #11369, #533 ) ;
#11123=CIRCLE ( 'NONE', #5399, 4.099999999999999645 ) ;
#11156=( NAMED_UNIT ( * ) PLANE_ANGLE_UNIT ( ) SI_UNIT ( $, .RADIAN. ) );
#11164=CYLINDRICAL_SURFACE ( 'NONE', #5842, 8.250000000000003553 ) ;
#11180=EDGE_CURVE ( 'NONE', #3632, #10657, #15103, .T. ) ;
#11186=DIRECTION ( 'NONE',  ( -6.123237831918399306E-17, 1.569224110909209817E-30, 1.000000000000000000 ) ) ;
#11214=VERTEX_POINT ( 'NONE', #14984 ) ;
#11219=FACE_OUTER_BOUND ( 'NONE', #12589, .T. ) ;
#11266=DIRECTION ( 'NONE',  ( 0.0007613694435018767380, -0.9999997101582432935, 0.000000000000000000 ) ) ;
#11272=FACE_BOUND ( 'NONE', #16019, .T. ) ;
#11338=FACE_BOUND ( 'NONE', #18209, .T. ) ;
#11369=DIRECTION ( 'NONE',  ( 6.123237831918399306E-17, -9.341417679122849747E-31, -1.000000000000000000 ) ) ;
#11485=CARTESIAN_POINT ( 'NONE',  ( -26.99999999999960210, -31.09999999999999787, 21.50000000000000000 ) ) ;
#11551=EDGE_CURVE ( 'NONE', #6032, #5808, #5233, .T. ) ;
#11566=CARTESIAN_POINT ( 'NONE',  ( -22.99999999999959854, -19.33065833018789803, -25.00000000000000000 ) ) ;
#11589=DIRECTION ( 'NONE',  ( -1.296622928517387947E-46, 1.000000000000000000, -1.557192143389729909E-30 ) ) ;
#11612=AXIS2_PLACEMENT_3D ( 'NONE', #6756, #1149, #6509 ) ;
#11651=ORIENTED_EDGE ( 'NONE', *, *, #9104, .T. ) ;
#11664=DIRECTION ( 'NONE',  ( -1.000000000000000000, 0.000000000000000000, 0.000000000000000000 ) ) ;
#11679=DIRECTION ( 'NONE',  ( 6.123237831918409167E-17, -1.613784273878194890E-30, -1.000000000000000000 ) ) ;
#11688=AXIS2_PLACEMENT_3D ( 'NONE', #22922, #11679, #13547 ) ;
#11738=DIRECTION ( 'NONE',  ( 0.000000000000000000, -1.000000000000000000, 0.000000000000000000 ) ) ;
#11772=CARTESIAN_POINT ( 'NONE',  ( 43.84419854219520118, 9.774809681453278998, 21.49999999999999289 ) ) ;
#11803=LINE ( 'NONE', #13677, #13379 ) ;
#11940=FACE_OUTER_BOUND ( 'NONE', #5964, .T. ) ;
#11942=EDGE_CURVE ( 'NONE', #16977, #5808, #15032, .T. ) ;
#12038=LINE ( 'NONE', #15572, #16785 ) ;
#12055=EDGE_CURVE ( 'NONE', #11110, #3632, #21319, .T. ) ;
#12077=DIRECTION ( 'NONE',  ( 6.123237831918409167E-17, -1.616838880122404932E-30, -1.000000000000000000 ) ) ;
#12078=VECTOR ( 'NONE', #8627, 1000.000000000000000 ) ;
#12135=EDGE_CURVE ( 'NONE', #290, #9398, #20846, .T. ) ;
#12341=ORIENTED_EDGE ( 'NONE', *, *, #8732, .T. ) ;
#12363=ORIENTED_EDGE ( 'NONE', *, *, #18643, .F. ) ;
#12374=ORIENTED_EDGE ( 'NONE', *, *, #20825, .F. ) ;
#12380=CARTESIAN_POINT ( 'NONE',  ( -26.99999999999959854, -19.33065833018799751, 21.49999999999999289 ) ) ;
#12441=ORIENTED_EDGE ( 'NONE', *, *, #5469, .F. ) ;
#12490=DIRECTION ( 'NONE',  ( 1.320147222947482081E-46, -2.155962677239134989E-30, -1.000000000000000000 ) ) ;
#12589=EDGE_LOOP ( 'NONE', ( #7434, #8194, #10714, #19579 ) ) ;
#12600=CARTESIAN_POINT ( 'NONE',  ( 43.84419854219520829, 9.774809681453278998, -65.86501949894326913 ) ) ;
#12618=ORIENTED_EDGE ( 'NONE', *, *, #4970, .F. ) ;
#12698=VERTEX_POINT ( 'NONE', #10272 ) ;
#12732=ORIENTED_EDGE ( 'NONE', *, *, #4050, .F. ) ;
#12739=AXIS2_PLACEMENT_3D ( 'NONE', #2569, #13380, #415 ) ;
#12764=EDGE_CURVE ( 'NONE', #19959, #8630, #19626, .T. ) ;
#12796=DIRECTION ( 'NONE',  ( -0.6660003063074659835, 0.7459514675891198987, 0.000000000000000000 ) ) ;
#12871=LINE ( 'NONE', #10993, #21510 ) ;
#12908=PLANE ( 'NONE',  #17016 ) ;
#12923=ORIENTED_EDGE ( 'NONE', *, *, #14381, .T. ) ;
#13001=VECTOR ( 'NONE', #8019, 1000.000000000000000 ) ;
#13024=DIRECTION ( 'NONE',  ( 6.123237831918399306E-17, -9.341417679122849747E-31, -1.000000000000000000 ) ) ;
#13058=DIRECTION ( 'NONE',  ( -1.000000000000000000, 0.000000000000000000, -0.000000000000000000 ) ) ;
#13076=EDGE_LOOP ( 'NONE', ( #9071, #7818, #7936, #1431, #2581, #21201 ) ) ;
#13134=CARTESIAN_POINT ( 'NONE',  ( 35.59419854219520118, 9.774809681453278998, 25.00000000000000000 ) ) ;
#13148=EDGE_LOOP ( 'NONE', ( #2111, #17094, #10176, #6027 ) ) ;
#13171=CARTESIAN_POINT ( 'NONE',  ( 35.59419854219520118, 9.774809681453278998, 21.49999999999999289 ) ) ;
#13174=ADVANCED_FACE ( 'NONE', ( #22799 ), #2749, .F. ) ;
#13196=EDGE_CURVE ( 'NONE', #2666, #13324, #6405, .T. ) ;
#13209=VECTOR ( 'NONE', #17180, 1000.000000000000000 ) ;
#13230=DIRECTION ( 'NONE',  ( 1.320147222947482081E-46, -2.155962677239134989E-30, -1.000000000000000000 ) ) ;
#13231=DIRECTION ( 'NONE',  ( 6.123237831918399306E-17, -1.569224110909209817E-30, -1.000000000000000000 ) ) ;
#13232=VECTOR ( 'NONE', #9005, 1000.000000000000000 ) ;
#13261=LINE ( 'NONE', #16934, #20994 ) ;
#13270=EDGE_CURVE ( 'NONE', #8287, #3632, #7112, .T. ) ;
#13324=VERTEX_POINT ( 'NONE', #2096 ) ;
#13379=VECTOR ( 'NONE', #3104, 1000.000000000000000 ) ;
#13380=DIRECTION ( 'NONE',  ( 0.000000000000000000, 0.000000000000000000, 1.000000000000000000 ) ) ;
#13396=UNCERTAINTY_MEASURE_WITH_UNIT (LENGTH_MEASURE( 1.000000000000000082E-05 ), #9824, 'distance_accuracy_value', 'NONE');
#13401=ADVANCED_FACE ( 'NONE', ( #23467 ), #12908, .T. ) ;
#13459=EDGE_CURVE ( 'NONE', #8556, #20891, #20424, .T. ) ;
#13494=PRODUCT_DEFINITION_SHAPE ( 'NONE', 'NONE',  #9377 ) ;
#13547=DIRECTION ( 'NONE',  ( -0.6660003063074659835, 0.7459514675891198987, 0.000000000000000000 ) ) ;
#13552=CARTESIAN_POINT ( 'NONE',  ( -25.00842861987479893, -15.87143667223269894, 23.00000000000000000 ) ) ;
#13591=EDGE_CURVE ( 'NONE', #22023, #8287, #17304, .T. ) ;
#13615=ADVANCED_BREP_SHAPE_REPRESENTATION ( '', ( #17052, #12739 ), #1341 ) ;
#13616=ADVANCED_FACE ( 'NONE', ( #6848 ), #3037, .T. ) ;
#13669=DIRECTION ( 'NONE',  ( -6.123237831918669245E-17, 0.000000000000000000, 1.000000000000000000 ) ) ;
#13677=CARTESIAN_POINT ( 'NONE',  ( -25.00842861987479893, -15.87143667223269894, -23.00000000000000000 ) ) ;
#13716=EDGE_CURVE ( 'NONE', #22023, #6032, #22872, .T. ) ;
#13734=CARTESIAN_POINT ( 'NONE',  ( 43.84419854219520829, -33.09999999999999432, -21.50000000000000000 ) ) ;
#13786=CIRCLE ( 'NONE', #2024, 3.999999999999998668 ) ;
#13787=ORIENTED_EDGE ( 'NONE', *, *, #23443, .T. ) ;
#13802=DIRECTION ( 'NONE',  ( -0.5021071549687909918, 0.8648054144888007722, -3.074521526981951182E-17 ) ) ;
#13803=LINE ( 'NONE', #15446, #10160 ) ;
#13811=VECTOR ( 'NONE', #18935, 1000.000000000000000 ) ;
#13895=ORIENTED_EDGE ( 'NONE', *, *, #21731, .T. ) ;
#13976=PLANE ( 'NONE',  #6984 ) ;
#14112=CARTESIAN_POINT ( 'NONE',  ( 39.69419854219519550, 9.774809681453278998, 25.00000000000000000 ) ) ;
#14117=AXIS2_PLACEMENT_3D ( 'NONE', #14847, #4292, #4044 ) ;
#14195=SHAPE_DEFINITION_REPRESENTATION ( #13494, #5348 ) ;
#14288=DIRECTION ( 'NONE',  ( -0.000000000000000000, -0.000000000000000000, 1.000000000000000000 ) ) ;
#14323=DIRECTION ( 'NONE',  ( -1.000000000000000000, 0.000000000000000000, 0.000000000000000000 ) ) ;
#14381=EDGE_CURVE ( 'NONE', #11110, #719, #7285, .T. ) ;
#14384=DIRECTION ( 'NONE',  ( 0.000000000000000000, 0.000000000000000000, -1.000000000000000000 ) ) ;
#14432=AXIS2_PLACEMENT_3D ( 'NONE', #13552, #13802, #13669 ) ;
#14475=ORIENTED_EDGE ( 'NONE', *, *, #13591, .F. ) ;
#14481=CYLINDRICAL_SURFACE ( 'NONE', #22210, 4.099999999999999645 ) ;
#14509=CARTESIAN_POINT ( 'NONE',  ( -26.99999999999959854, -33.09999999999999432, 25.00000000000000000 ) ) ;
#14519=VECTOR ( 'NONE', #7096, 1000.000000000000000 ) ;
#14530=VECTOR ( 'NONE', #7137, 1000.000000000000000 ) ;
#14576=ADVANCED_FACE ( 'NONE', ( #491 ), #18564, .T. ) ;
#14578=ORIENTED_EDGE ( 'NONE', *, *, #6086, .T. ) ;
#14587=ADVANCED_FACE ( 'NONE', ( #11338, #2156 ), #6073, .F. ) ;
#14651=AXIS2_PLACEMENT_3D ( 'NONE', #1416, #5112, #7134 ) ;
#14659=VECTOR ( 'NONE', #15044, 1000.000000000000000 ) ;
#14708=CARTESIAN_POINT ( 'NONE',  ( 31.49419854219519976, 9.774809681453278998, 23.00000000000000000 ) ) ;
#14829=EDGE_CURVE ( 'NONE', #4562, #11214, #13803, .T. ) ;
#14847=CARTESIAN_POINT ( 'NONE',  ( 35.59419854219520118, 9.774809681453278998, -23.00000000000000000 ) ) ;
#14860=ORIENTED_EDGE ( 'NONE', *, *, #15824, .T. ) ;
#14879=FACE_OUTER_BOUND ( 'NONE', #14980, .T. ) ;
#14880=DIRECTION ( 'NONE',  ( -1.000000000000000000, 0.000000000000000000, 0.000000000000000000 ) ) ;
#14887=CIRCLE ( 'NONE', #6157, 4.099999999999999645 ) ;
#14923=SHAPE_REPRESENTATION_RELATIONSHIP ( 'NONE' , 'NONE' ,  #5348, #13615 ) ;
#14980=EDGE_LOOP ( 'NONE', ( #7966, #6835, #2521, #17466, #21333 ) ) ;
#14984=CARTESIAN_POINT ( 'NONE',  ( -25.00842861987479893, -15.87143667223269894, 25.00000000000000000 ) ) ;
#14991=ORIENTED_EDGE ( 'NONE', *, *, #23443, .F. ) ;
#15032=LINE ( 'NONE', #4468, #22661 ) ;
#15044=DIRECTION ( 'NONE',  ( 0.000000000000000000, -2.899485473084796609E-46, -1.000000000000000000 ) ) ;
#15103=LINE ( 'NONE', #841, #6336 ) ;
#15111=CARTESIAN_POINT ( 'NONE',  ( 35.59419854219520118, 9.774809681453278998, -25.00000000000000000 ) ) ;
#15135=EDGE_CURVE ( 'NONE', #8287, #6032, #690, .T. ) ;
#15147=AXIS2_PLACEMENT_3D ( 'NONE', #9759, #22313, #11664 ) ;
#15226=CARTESIAN_POINT ( 'NONE',  ( -25.00842861987479182, -15.87143667223269539, 21.49999999999999289 ) ) ;
#15299=VECTOR ( 'NONE', #13230, 1000.000000000000000 ) ;
#15301=DIRECTION ( 'NONE',  ( 0.6660003063074656504, -0.7459514675891198987, 0.000000000000000000 ) ) ;
#15446=CARTESIAN_POINT ( 'NONE',  ( -25.00842861987479893, -15.87143667223269894, 23.00000000000000000 ) ) ;
#15454=EDGE_LOOP ( 'NONE', ( #2698, #14578 ) ) ;
#15497=VERTEX_POINT ( 'NONE', #14112 ) ;
#15504=CARTESIAN_POINT ( 'NONE',  ( -26.99999999999959854, -30.09999999999999787, 25.00000000000000000 ) ) ;
#15541=CARTESIAN_POINT ( 'NONE',  ( 39.69419854219519550, 9.774809681453278998, -25.00000000000000000 ) ) ;
#15543=CIRCLE ( 'NONE', #16301, 8.250000000000000000 ) ;
#15544=ORIENTED_EDGE ( 'NONE', *, *, #12055, .T. ) ;
#15561=AXIS2_PLACEMENT_3D ( 'NONE', #5763, #13024, #1403 ) ;
#15572=CARTESIAN_POINT ( 'NONE',  ( -26.99999999999959854, 8.392275869980100359E-122, 21.49999999999999289 ) ) ;
#15607=ORIENTED_EDGE ( 'NONE', *, *, #12135, .F. ) ;
#15656=CIRCLE ( 'NONE', #11116, 4.099999999999999645 ) ;
#15694=DIRECTION ( 'NONE',  ( -1.000000000000000000, 0.000000000000000000, 0.000000000000000000 ) ) ;
#15699=ORIENTED_EDGE ( 'NONE', *, *, #11551, .F. ) ;
#15715=DIRECTION ( 'NONE',  ( 6.123237831918399306E-17, -1.586917373610080078E-30, -1.000000000000000000 ) ) ;
#15751=DIRECTION ( 'NONE',  ( 0.000000000000000000, -1.000000000000000000, -1.734723475976808278E-15 ) ) ;
#15800=CIRCLE ( 'NONE', #7461, 3.999999999999998668 ) ;
#15805=DIRECTION ( 'NONE',  ( 8.410780489584519664E-16, -1.000000000000000000, 0.000000000000000000 ) ) ;
#15824=EDGE_CURVE ( 'NONE', #8556, #19315, #3246, .T. ) ;
#15834=VECTOR ( 'NONE', #23199, 1000.000000000000000 ) ;
#15844=ORIENTED_EDGE ( 'NONE', *, *, #20920, .T. ) ;
#15871=DIRECTION ( 'NONE',  ( -4.040376328279780192E-15, 1.000000000000000000, 0.000000000000000000 ) ) ;
#15881=PLANE ( 'NONE',  #11612 ) ;
#15965=LINE ( 'NONE', #19421, #15834 ) ;
#15989=VECTOR ( 'NONE', #16724, 999.9999999999998863 ) ;
#16018=VERTEX_POINT ( 'NONE', #18332 ) ;
#16019=EDGE_LOOP ( 'NONE', ( #21875, #9011 ) ) ;
#16109=ORIENTED_EDGE ( 'NONE', *, *, #18232, .T. ) ;
#16120=CARTESIAN_POINT ( 'NONE',  ( 43.84267580286685018, -31.09999999999999787, -21.50000000000000000 ) ) ;
#16224=CARTESIAN_POINT ( 'NONE',  ( 35.59419854219520118, 9.774809681453278998, 21.49999999999999289 ) ) ;
#16234=CARTESIAN_POINT ( 'NONE',  ( 0.5868595415223712974, -1.010778882616216512, 21.49999999999999289 ) ) ;
#16245=EDGE_CURVE ( 'NONE', #10657, #17474, #12038, .T. ) ;
#16251=ORIENTED_EDGE ( 'NONE', *, *, #13716, .F. ) ;
#16301=AXIS2_PLACEMENT_3D ( 'NONE', #8029, #18952, #17291 ) ;
#16312=VECTOR ( 'NONE', #18440, 1000.000000000000000 ) ;
#16445=EDGE_LOOP ( 'NONE', ( #15607, #21928, #4884, #18461, #5578, #20831 ) ) ;
#16464=DIRECTION ( 'NONE',  ( -0.5021071549687909918, 0.8648054144888007722, -3.074521526981951182E-17 ) ) ;
#16634=DIRECTION ( 'NONE',  ( -2.977235988022386522E-185, 9.605990953944227443E-124, 1.000000000000000000 ) ) ;
#16659=CARTESIAN_POINT ( 'NONE',  ( 8.284960688207139157, -8.610885316305260773, -25.00000000000000000 ) ) ;
#16667=ORIENTED_EDGE ( 'NONE', *, *, #13716, .T. ) ;
#16698=APPLICATION_CONTEXT ( 'configuration controlled 3d designs of mechanical parts and assemblies' ) ;
#16724=DIRECTION ( 'NONE',  ( 0.0007613694435018767380, -0.9999997101582432935, 0.000000000000000000 ) ) ;
#16785=VECTOR ( 'NONE', #19032, 1000.000000000000000 ) ;
#16831=DIRECTION ( 'NONE',  ( 8.673617379884035472E-16, -1.000000000000000000, 0.000000000000000000 ) ) ;
#16934=CARTESIAN_POINT ( 'NONE',  ( 43.84419854219520829, 0.000000000000000000, 25.00000000000000000 ) ) ;
#16942=CARTESIAN_POINT ( 'NONE',  ( 43.84419854219520829, -31.09999999999999787, -21.49999999999999645 ) ) ;
#16977=VERTEX_POINT ( 'NONE', #21473 ) ;
#17016=AXIS2_PLACEMENT_3D ( 'NONE', #3757, #16464, #10681 ) ;
#17052=MANIFOLD_SOLID_BREP ( 'Boss-Extrude4', #9913 ) ;
#17082=PRODUCT ( 'Fixed base', 'Fixed base', '', ( #10180 ) ) ;
#17094=ORIENTED_EDGE ( 'NONE', *, *, #22988, .T. ) ;
#17149=FACE_BOUND ( 'NONE', #15454, .T. ) ;
#17180=DIRECTION ( 'NONE',  ( 5.039379565342698073E-16, -1.000000000000000000, 0.000000000000000000 ) ) ;
#17206=VERTEX_POINT ( 'NONE', #165 ) ;
#17221=VERTEX_POINT ( 'NONE', #10901 ) ;
#17277=CARTESIAN_POINT ( 'NONE',  ( 31.45181451370270054, 16.90945435098589655, 25.00000000000000000 ) ) ;
#17291=DIRECTION ( 'NONE',  ( -1.000000000000000000, 0.000000000000000000, 0.000000000000000000 ) ) ;
#17304=LINE ( 'NONE', #10307, #12078 ) ;
#17314=ORIENTED_EDGE ( 'NONE', *, *, #16245, .F. ) ;
#17334=ORIENTED_EDGE ( 'NONE', *, *, #11551, .T. ) ;
#17390=VECTOR ( 'NONE', #7280, 999.9999999999998863 ) ;
#17405=CARTESIAN_POINT ( 'NONE',  ( 35.59419854219520118, 9.774809681453278998, -23.00000000000000000 ) ) ;
#17466=ORIENTED_EDGE ( 'NONE', *, *, #13270, .T. ) ;
#17474=VERTEX_POINT ( 'NONE', #12380 ) ;
#17509=ORIENTED_EDGE ( 'NONE', *, *, #22295, .F. ) ;
#17539=ORIENTED_EDGE ( 'NONE', *, *, #21686, .F. ) ;
#17614=ORIENTED_EDGE ( 'NONE', *, *, #20920, .F. ) ;
#17779=ORIENTED_EDGE ( 'NONE', *, *, #13459, .T. ) ;
#17836=VERTEX_POINT ( 'NONE', #11772 ) ;
#17889=CARTESIAN_POINT ( 'NONE',  ( -26.99999999999959854, -30.09999999999999787, 23.00000000000000000 ) ) ;
#17891=VERTEX_POINT ( 'NONE', #15541 ) ;
#17929=ORIENTED_EDGE ( 'NONE', *, *, #21461, .T. ) ;
#17948=PRODUCT_DEFINITION_FORMATION_WITH_SPECIFIED_SOURCE ( 'ANY', '', #17082, .NOT_KNOWN. ) ;
#17983=DIRECTION ( 'NONE',  ( -6.123237831918399306E-17, 1.569224110909209817E-30, 1.000000000000000000 ) ) ;
#18010=DESIGN_CONTEXT ( 'detailed design', #22640, 'design' ) ;
#18097=ORIENTED_EDGE ( 'NONE', *, *, #13459, .F. ) ;
#18105=CARTESIAN_POINT ( 'NONE',  ( 39.69419854219519550, 9.774809681453278998, 21.49999999999999289 ) ) ;
#18126=AXIS2_PLACEMENT_3D ( 'NONE', #21324, #1361, #23213 ) ;
#18178=ORIENTED_EDGE ( 'NONE', *, *, #919, .F. ) ;
#18192=VECTOR ( 'NONE', #5831, 999.9999999999998863 ) ;
#18193=ORIENTED_EDGE ( 'NONE', *, *, #8913, .T. ) ;
#18209=EDGE_LOOP ( 'NONE', ( #20419, #3957 ) ) ;
#18217=DIRECTION ( 'NONE',  ( 4.040376328279780192E-15, -1.000000000000000000, 1.816625962794309743E-30 ) ) ;
#18232=EDGE_CURVE ( 'NONE', #20891, #17891, #19932, .T. ) ;
#18243=DIRECTION ( 'NONE',  ( -6.123237831918399306E-17, 2.152213273084510109E-30, 1.000000000000000000 ) ) ;
#18277=ORIENTED_EDGE ( 'NONE', *, *, #4050, .T. ) ;
#18307=AXIS2_PLACEMENT_3D ( 'NONE', #16224, #2079, #10905 ) ;
#18332=CARTESIAN_POINT ( 'NONE',  ( 31.49419854219519976, 9.774809681453278998, 25.00000000000000000 ) ) ;
#18373=LINE ( 'NONE', #5644, #3518 ) ;
#18383=( NAMED_UNIT ( * ) SI_UNIT ( $, .STERADIAN. ) SOLID_ANGLE_UNIT ( ) );
#18385=CARTESIAN_POINT ( 'NONE',  ( 35.59419854219520118, 9.774809681453278998, 23.00000000000000000 ) ) ;
#18421=ADVANCED_FACE ( 'NONE', ( #10550 ), #13976, .T. ) ;
#18440=DIRECTION ( 'NONE',  ( 1.000000000000000000, 9.794583108699330061E-17, 0.000000000000000000 ) ) ;
#18461=ORIENTED_EDGE ( 'NONE', *, *, #13196, .F. ) ;
#18504=DIRECTION ( 'NONE',  ( -5.742930707022404410E-47, 9.378911720669089789E-31, 1.000000000000000000 ) ) ;
#18564=PLANE ( 'NONE',  #21113 ) ;
#18565=EDGE_CURVE ( 'NONE', #17206, #17836, #10201, .T. ) ;
#18569=VERTEX_POINT ( 'NONE', #5529 ) ;
#18643=EDGE_CURVE ( 'NONE', #1017, #17221, #9601, .T. ) ;
#18662=EDGE_CURVE ( 'NONE', #19315, #17891, #14887, .T. ) ;
#18726=LINE ( 'NONE', #5880, #13001 ) ;
#18792=CYLINDRICAL_SURFACE ( 'NONE', #14117, 4.099999999999999645 ) ;
#18802=CARTESIAN_POINT ( 'NONE',  ( 35.59419854219520118, 9.774809681453278998, 23.00000000000000000 ) ) ;
#18816=DIRECTION ( 'NONE',  ( 1.000000000000000000, -1.555753819465284865E-62, -8.326672684687908612E-17 ) ) ;
#18925=CARTESIAN_POINT ( 'NONE',  ( 43.81210844073630994, 9.047859270861110303, -21.50000000000000000 ) ) ;
#18935=DIRECTION ( 'NONE',  ( 1.000000000000000000, 9.794583108699330061E-17, 0.000000000000000000 ) ) ;
#18938=EDGE_CURVE ( 'NONE', #15497, #16018, #15656, .T. ) ;
#18952=DIRECTION ( 'NONE',  ( 0.000000000000000000, 0.000000000000000000, -1.000000000000000000 ) ) ;
#19032=DIRECTION ( 'NONE',  ( 0.000000000000000000, 1.000000000000000000, -9.605990953944227443E-124 ) ) ;
#19043=ORIENTED_EDGE ( 'NONE', *, *, #14829, .F. ) ;
#19123=AXIS2_PLACEMENT_3D ( 'NONE', #16659, #2306, #20471 ) ;
#19223=AXIS2_PLACEMENT_3D ( 'NONE', #20505, #2691, #16831 ) ;
#19315=VERTEX_POINT ( 'NONE', #4323 ) ;
#19360=FACE_OUTER_BOUND ( 'NONE', #2106, .T. ) ;
#19405=CARTESIAN_POINT ( 'NONE',  ( 31.49419854219519976, 9.774809681453278998, -23.00000000000000000 ) ) ;
#19421=CARTESIAN_POINT ( 'NONE',  ( -26.99999999999959854, -31.09999999999999787, 21.50000000000000000 ) ) ;
#19450=ADVANCED_FACE ( 'NONE', ( #14879 ), #4072, .T. ) ;
#19452=CIRCLE ( 'NONE', #10758, 4.100000000000000533 ) ;
#19541=DIRECTION ( 'NONE',  ( -4.040376328279780192E-15, 1.000000000000000000, -1.816625962794309743E-30 ) ) ;
#19579=ORIENTED_EDGE ( 'NONE', *, *, #18938, .F. ) ;
#19626=LINE ( 'NONE', #10866, #17390 ) ;
#19654=ADVANCED_FACE ( 'NONE', ( #22693, #11940 ), #2882, .F. ) ;
#19698=ORIENTED_EDGE ( 'NONE', *, *, #7741, .F. ) ;
#19841=CARTESIAN_POINT ( 'NONE',  ( 8.284960688207149815, -8.610885316305250115, 25.00000000000000000 ) ) ;
#19899=LINE ( 'NONE', #7086, #519 ) ;
#19916=ADVANCED_FACE ( 'NONE', ( #8291 ), #6386, .T. ) ;
#19932=LINE ( 'NONE', #10931, #20240 ) ;
#19959=VERTEX_POINT ( 'NONE', #9843 ) ;
#20240=VECTOR ( 'NONE', #7576, 1000.000000000000000 ) ;
#20253=PLANE ( 'NONE',  #19123 ) ;
#20292=EDGE_CURVE ( 'NONE', #6032, #6621, #18373, .T. ) ;
#20358=FACE_OUTER_BOUND ( 'NONE', #13076, .T. ) ;
#20379=CARTESIAN_POINT ( 'NONE',  ( 31.45181451370271475, 16.90945435098595340, 21.49999999999999289 ) ) ;
#20408=DIRECTION ( 'NONE',  ( 0.000000000000000000, -1.000000000000000000, 0.000000000000000000 ) ) ;
#20419=ORIENTED_EDGE ( 'NONE', *, *, #7093, .T. ) ;
#20424=CIRCLE ( 'NONE', #6013, 4.099999999999999645 ) ;
#20434=EDGE_LOOP ( 'NONE', ( #12363, #18193, #12441, #22542 ) ) ;
#20446=DIRECTION ( 'NONE',  ( -1.000000000000000000, 0.000000000000000000, 0.000000000000000000 ) ) ;
#20450=DIRECTION ( 'NONE',  ( -6.123237831918399306E-17, 1.569224110909209817E-30, 1.000000000000000000 ) ) ;
#20471=DIRECTION ( 'NONE',  ( 1.000000000000000000, 6.123237831918438750E-17, -1.555753819465284865E-62 ) ) ;
#20505=CARTESIAN_POINT ( 'NONE',  ( -22.99999999999959854, -19.33065833018789803, 21.49999999999999289 ) ) ;
#20516=ORIENTED_EDGE ( 'NONE', *, *, #9544, .F. ) ;
#20531=ADVANCED_FACE ( 'NONE', ( #8507 ), #23075, .T. ) ;
#20579=CARTESIAN_POINT ( 'NONE',  ( -26.99999999999959854, -31.09999999999999787, -22.00000000000000000 ) ) ;
#20599=LINE ( 'NONE', #22357, #13811 ) ;
#20677=CIRCLE ( 'NONE', #5511, 8.250000000000001776 ) ;
#20825=EDGE_CURVE ( 'NONE', #18569, #16977, #4540, .T. ) ;
#20831=ORIENTED_EDGE ( 'NONE', *, *, #21029, .F. ) ;
#20846=LINE ( 'NONE', #15504, #295 ) ;
#20891=VERTEX_POINT ( 'NONE', #22346 ) ;
#20920=EDGE_CURVE ( 'NONE', #21997, #2666, #2647, .T. ) ;
#20966=VECTOR ( 'NONE', #2551, 1000.000000000000000 ) ;
#20994=VECTOR ( 'NONE', #11738, 1000.000000000000000 ) ;
#21029=EDGE_CURVE ( 'NONE', #9398, #11214, #13786, .T. ) ;
#21113=AXIS2_PLACEMENT_3D ( 'NONE', #9535, #4060, #7985 ) ;
#21142=PLANE ( 'NONE',  #14432 ) ;
#21201=ORIENTED_EDGE ( 'NONE', *, *, #1275, .F. ) ;
#21258=AXIS2_PLACEMENT_3D ( 'NONE', #19841, #18504, #7143 ) ;
#21319=LINE ( 'NONE', #4706, #13209 ) ;
#21324=CARTESIAN_POINT ( 'NONE',  ( 43.81897180516431689, 0.03336243584794939404, -21.50000000000000000 ) ) ;
#21333=ORIENTED_EDGE ( 'NONE', *, *, #11180, .T. ) ;
#21442=VECTOR ( 'NONE', #7219, 1000.000000000000114 ) ;
#21461=EDGE_CURVE ( 'NONE', #12698, #719, #15800, .T. ) ;
#21473=CARTESIAN_POINT ( 'NONE',  ( 43.81210844073630284, 9.047859270861110303, -25.00000000000000000 ) ) ;
#21479=CARTESIAN_POINT ( 'NONE',  ( 86.89068504225697609, -33.09999999999999432, -21.50000000000000000 ) ) ;
#21510=VECTOR ( 'NONE', #18217, 1000.000000000000000 ) ;
#21512=VECTOR ( 'NONE', #12490, 1000.000000000000000 ) ;
#21517=CARTESIAN_POINT ( 'NONE',  ( -26.99999999999959854, -19.33065833018799751, -23.00000000000000000 ) ) ;
#21542=DIRECTION ( 'NONE',  ( -6.123237831918399306E-17, 1.569224110909209817E-30, 1.000000000000000000 ) ) ;
#21571=VECTOR ( 'NONE', #23124, 1000.000000000000000 ) ;
#21613=ORIENTED_EDGE ( 'NONE', *, *, #18662, .F. ) ;
#21686=EDGE_CURVE ( 'NONE', #17206, #22023, #6377, .T. ) ;
#21731=EDGE_CURVE ( 'NONE', #17474, #4562, #5566, .T. ) ;
#21759=CARTESIAN_POINT ( 'NONE',  ( -26.99999999999959854, -19.33065833018799751, 25.00000000000000000 ) ) ;
#21840=ORIENTED_EDGE ( 'NONE', *, *, #9544, .T. ) ;
#21875=ORIENTED_EDGE ( 'NONE', *, *, #5469, .T. ) ;
#21883=LINE ( 'NONE', #4078, #258 ) ;
#21928=ORIENTED_EDGE ( 'NONE', *, *, #1764, .T. ) ;
#21953=ORIENTED_EDGE ( 'NONE', *, *, #4069, .T. ) ;
#21976=DIRECTION ( 'NONE',  ( -6.123237831918399306E-17, 1.569224110909209817E-30, 1.000000000000000000 ) ) ;
#21994=EDGE_LOOP ( 'NONE', ( #17929, #9746, #5936, #3612 ) ) ;
#21997=VERTEX_POINT ( 'NONE', #20379 ) ;
#22023=VERTEX_POINT ( 'NONE', #650 ) ;
#22050=ORIENTED_EDGE ( 'NONE', *, *, #20292, .F. ) ;
#22140=CARTESIAN_POINT ( 'NONE',  ( -26.99999999999959854, -33.09999999999999432, -22.00000000000000000 ) ) ;
#22180=DIRECTION ( 'NONE',  ( -6.123237831918409167E-17, 1.613784273878194890E-30, 1.000000000000000000 ) ) ;
#22210=AXIS2_PLACEMENT_3D ( 'NONE', #9025, #11186, #9262 ) ;
#22295=EDGE_CURVE ( 'NONE', #10657, #17206, #15965, .T. ) ;
#22313=DIRECTION ( 'NONE',  ( 0.000000000000000000, 0.000000000000000000, -1.000000000000000000 ) ) ;
#22346=CARTESIAN_POINT ( 'NONE',  ( 39.69419854219519550, 9.774809681453278998, -21.50000000000000000 ) ) ;
#22350=CIRCLE ( 'NONE', #4157, 4.099999999999999645 ) ;
#22357=CARTESIAN_POINT ( 'NONE',  ( 3.242007008979478005E-15, -33.09999999999999432, -25.00000000000000000 ) ) ;
#22452=DIRECTION ( 'NONE',  ( 6.123237831918399306E-17, -1.569224110909209817E-30, -1.000000000000000000 ) ) ;
#22456=CYLINDRICAL_SURFACE ( 'NONE', #1897, 4.099999999999999645 ) ;
#22542=ORIENTED_EDGE ( 'NONE', *, *, #22896, .F. ) ;
#22640=APPLICATION_CONTEXT ( 'configuration controlled 3d designs of mechanical parts and assemblies' ) ;
#22650=ORIENTED_EDGE ( 'NONE', *, *, #5000, .F. ) ;
#22661=VECTOR ( 'NONE', #11266, 999.9999999999998863 ) ;
#22693=FACE_BOUND ( 'NONE', #2880, .T. ) ;
#22787=ORIENTED_EDGE ( 'NONE', *, *, #13270, .F. ) ;
#22799=FACE_OUTER_BOUND ( 'NONE', #6209, .T. ) ;
#22803=DIRECTION ( 'NONE',  ( -6.123237831918399306E-17, 1.569224110909209817E-30, 1.000000000000000000 ) ) ;
#22804=EDGE_LOOP ( 'NONE', ( #9483, #9270, #12923, #3491, #18277, #8961, #20516, #17314 ) ) ;
#22818=ORIENTED_EDGE ( 'NONE', *, *, #15135, .T. ) ;
#22872=LINE ( 'NONE', #13734, #7496 ) ;
#22896=EDGE_CURVE ( 'NONE', #17221, #16018, #7475, .T. ) ;
#22922=CARTESIAN_POINT ( 'NONE',  ( 35.59419854219520118, 9.774809681453278998, 25.00000000000000000 ) ) ;
#22988=EDGE_CURVE ( 'NONE', #16977, #115, #20677, .T. ) ;
#23021=ORIENTED_EDGE ( 'NONE', *, *, #15824, .F. ) ;
#23026=AXIS2_PLACEMENT_3D ( 'NONE', #2627, #22452, #15694 ) ;
#23075=CYLINDRICAL_SURFACE ( 'NONE', #8460, 8.250000000000001776 ) ;
#23124=DIRECTION ( 'NONE',  ( 0.8648054144888007722, 0.5021071549687909918, 5.295409231245618283E-17 ) ) ;
#23141=ADVANCED_FACE ( 'NONE', ( #6870 ), #15881, .F. ) ;
#23145=PLANE ( 'NONE',  #21258 ) ;
#23199=DIRECTION ( 'NONE',  ( 1.000000000000000000, 1.296622928517386003E-46, -1.245534812201467949E-169 ) ) ;
#23213=DIRECTION ( 'NONE',  ( -0.0007613694435018768464, 0.9999997101582432935, 0.000000000000000000 ) ) ;
#23257=ORIENTED_EDGE ( 'NONE', *, *, #1764, .F. ) ;
#23306=ORIENTED_EDGE ( 'NONE', *, *, #13196, .T. ) ;
#23337=CARTESIAN_POINT ( 'NONE',  ( 43.84419854219520829, 8.392275869980100359E-122, 21.49999999999999289 ) ) ;
#23422=CARTESIAN_POINT ( 'NONE',  ( 35.59419854219520118, 9.774809681453278998, -21.50000000000000000 ) ) ;
#23428=EDGE_LOOP ( 'NONE', ( #22050, #16251, #17539, #2732, #10596, #12341 ) ) ;
#23443=EDGE_CURVE ( 'NONE', #4562, #21997, #9001, .T. ) ;
#23466=VERTEX_POINT ( 'NONE', #9462 ) ;
#23467=FACE_OUTER_BOUND ( 'NONE', #10036, .T. ) ;
#23543=COLOUR_RGB('Light Gray', 0.72549020, 0.75294118, 0.79215686);
#23544=FILL_AREA_STYLE_COLOUR('',#23543);
#23545=FILL_AREA_STYLE('',(#23544));
#23546=SURFACE_STYLE_FILL_AREA(#23545);
#23547=SURFACE_SIDE_STYLE('',(#23546));
#23548=SURFACE_STYLE_USAGE(.BOTH.,#23547);
#23549=PRESENTATION_STYLE_ASSIGNMENT((#23548));
#23597=STYLED_ITEM('',(#23549),#17052);
#23598=MECHANICAL_DESIGN_GEOMETRIC_PRESENTATION_REPRESENTATION('',(#23597),#1341);
ENDSEC;
END-ISO-10303-21;
